ISO-10303-21;
HEADER;
/* Generated by software containing ST-Developer
 * from STEP Tools, Inc. (www.steptools.com) 
 */

FILE_DESCRIPTION(
/* description */ ('Air blow-off nozzle station'),
/* implementation_level */ '2;1');

FILE_NAME(
/* name */ 'M5x14 Cap Screw.step',
/* time_stamp */ '2026-10-27T10:53:54-07:00',
/* author */ (''),
/* organization */ (''),
/* preprocessor_version */ 'ST-DEVELOPER v20.2',
/* originating_system */ 'Autodesk Translation Framework v15.17.0.0',
/* authorisation */ '');

FILE_SCHEMA (('AUTOMOTIVE_DESIGN { 1 0 10303 214 3 1 1 }'));
ENDSEC;

DATA;
#10=MECHANICAL_DESIGN_GEOMETRIC_PRESENTATION_REPRESENTATION('',(#248),#7897);
#151=ORIENTED_CLOSED_SHELL('',*,#4297,.F.);
#153=BREP_WITH_VOIDS('Body1',#4298,(#151));
#156=CONICAL_SURFACE('',#4823,0.4,0.785398163397448);
#157=CONICAL_SURFACE('',#4827,0.41,0.785398163397448);
#158=CONICAL_SURFACE('',#4831,0.26,0.463647609000806);
#198=SHAPE_REPRESENTATION_RELATIONSHIP('SRR','None',#8012,#223);
#223=ADVANCED_BREP_SHAPE_REPRESENTATION('',(#153),#7879);
#248=STYLED_ITEM('',(#8227),#153);
#329=FACE_BOUND('',#991,.T.);
#472=PLANE('',#4811);
#473=PLANE('',#4812);
#474=PLANE('',#4813);
#475=PLANE('',#4814);
#476=PLANE('',#4815);
#477=PLANE('',#4816);
#478=PLANE('',#4817);
#479=PLANE('',#4818);
#480=PLANE('',#4819);
#481=PLANE('',#4821);
#482=PLANE('',#4829);
#677=FACE_OUTER_BOUND('',#977,.T.);
#678=FACE_OUTER_BOUND('',#978,.T.);
#679=FACE_OUTER_BOUND('',#979,.T.);
#680=FACE_OUTER_BOUND('',#980,.T.);
#681=FACE_OUTER_BOUND('',#981,.T.);
#682=FACE_OUTER_BOUND('',#982,.T.);
#683=FACE_OUTER_BOUND('',#983,.T.);
#684=FACE_OUTER_BOUND('',#984,.T.);
#685=FACE_OUTER_BOUND('',#985,.T.);
#686=FACE_OUTER_BOUND('',#986,.T.);
#687=FACE_OUTER_BOUND('',#987,.T.);
#688=FACE_OUTER_BOUND('',#988,.T.);
#689=FACE_OUTER_BOUND('',#989,.T.);
#690=FACE_OUTER_BOUND('',#990,.T.);
#691=FACE_OUTER_BOUND('',#992,.T.);
#692=FACE_OUTER_BOUND('',#993,.T.);
#977=EDGE_LOOP('',(#3539,#3540,#3541,#3542));
#978=EDGE_LOOP('',(#3543,#3544,#3545,#3546));
#979=EDGE_LOOP('',(#3547,#3548,#3549,#3550));
#980=EDGE_LOOP('',(#3551,#3552,#3553,#3554));
#981=EDGE_LOOP('',(#3555,#3556,#3557,#3558));
#982=EDGE_LOOP('',(#3559,#3560,#3561,#3562));
#983=EDGE_LOOP('',(#3563,#3564,#3565,#3566,#3567,#3568));
#984=EDGE_LOOP('',(#3569,#3570,#3571,#3572,#3573,#3574));
#985=EDGE_LOOP('',(#3575));
#986=EDGE_LOOP('',(#3576));
#987=EDGE_LOOP('',(#3577,#3578,#3579,#3580));
#988=EDGE_LOOP('',(#3581,#3582,#3583,#3584));
#989=EDGE_LOOP('',(#3585,#3586,#3587,#3588));
#990=EDGE_LOOP('',(#3589));
#991=EDGE_LOOP('',(#3590));
#992=EDGE_LOOP('',(#3591,#3592,#3593,#3594));
#993=EDGE_LOOP('',(#3595,#3596,#3597,#3598));
#1372=LINE('',#7315,#1726);
#1373=LINE('',#7317,#1727);
#1374=LINE('',#7319,#1728);
#1375=LINE('',#7320,#1729);
#1376=LINE('',#7323,#1730);
#1377=LINE('',#7325,#1731);
#1378=LINE('',#7326,#1732);
#1379=LINE('',#7329,#1733);
#1380=LINE('',#7331,#1734);
#1381=LINE('',#7332,#1735);
#1382=LINE('',#7335,#1736);
#1383=LINE('',#7337,#1737);
#1384=LINE('',#7338,#1738);
#1385=LINE('',#7341,#1739);
#1386=LINE('',#7343,#1740);
#1387=LINE('',#7344,#1741);
#1388=LINE('',#7346,#1742);
#1389=LINE('',#7347,#1743);
#1390=LINE('',#7359,#1744);
#1391=LINE('',#7363,#1745);
#1392=LINE('',#7367,#1746);
#1393=LINE('',#7374,#1747);
#1394=LINE('',#7376,#1748);
#1726=VECTOR('',#5752,1.);
#1727=VECTOR('',#5753,1.);
#1728=VECTOR('',#5754,1.);
#1729=VECTOR('',#5755,1.);
#1730=VECTOR('',#5758,1.);
#1731=VECTOR('',#5759,1.);
#1732=VECTOR('',#5760,1.);
#1733=VECTOR('',#5763,1.);
#1734=VECTOR('',#5764,1.);
#1735=VECTOR('',#5765,1.);
#1736=VECTOR('',#5768,1.);
#1737=VECTOR('',#5769,1.);
#1738=VECTOR('',#5770,1.);
#1739=VECTOR('',#5773,1.);
#1740=VECTOR('',#5774,1.);
#1741=VECTOR('',#5775,1.);
#1742=VECTOR('',#5778,1.);
#1743=VECTOR('',#5779,1.);
#1744=VECTOR('',#5796,0.4);
#1745=VECTOR('',#5801,0.425);
#1746=VECTOR('',#5806,0.41);
#1747=VECTOR('',#5815,0.26);
#1748=VECTOR('',#5818,0.25);
#1917=CIRCLE('',#4820,0.24505);
#1918=CIRCLE('',#4822,0.375);
#1919=CIRCLE('',#4824,0.425);
#1920=CIRCLE('',#4826,0.425);
#1921=CIRCLE('',#4828,0.395);
#1922=CIRCLE('',#4830,0.27);
#1923=CIRCLE('',#4832,0.24505);
#2225=VERTEX_POINT('',#7313);
#2226=VERTEX_POINT('',#7314);
#2227=VERTEX_POINT('',#7316);
#2228=VERTEX_POINT('',#7318);
#2229=VERTEX_POINT('',#7322);
#2230=VERTEX_POINT('',#7324);
#2231=VERTEX_POINT('',#7328);
#2232=VERTEX_POINT('',#7330);
#2233=VERTEX_POINT('',#7334);
#2234=VERTEX_POINT('',#7336);
#2235=VERTEX_POINT('',#7340);
#2236=VERTEX_POINT('',#7342);
#2237=VERTEX_POINT('',#7351);
#2238=VERTEX_POINT('',#7354);
#2239=VERTEX_POINT('',#7357);
#2240=VERTEX_POINT('',#7361);
#2241=VERTEX_POINT('',#7365);
#2242=VERTEX_POINT('',#7369);
#2243=VERTEX_POINT('',#7372);
#2687=EDGE_CURVE('',#2225,#2226,#1372,.T.);
#2688=EDGE_CURVE('',#2226,#2227,#1373,.T.);
#2689=EDGE_CURVE('',#2227,#2228,#1374,.T.);
#2690=EDGE_CURVE('',#2225,#2228,#1375,.T.);
#2691=EDGE_CURVE('',#2226,#2229,#1376,.T.);
#2692=EDGE_CURVE('',#2229,#2230,#1377,.T.);
#2693=EDGE_CURVE('',#2230,#2227,#1378,.T.);
#2694=EDGE_CURVE('',#2229,#2231,#1379,.T.);
#2695=EDGE_CURVE('',#2231,#2232,#1380,.T.);
#2696=EDGE_CURVE('',#2232,#2230,#1381,.T.);
#2697=EDGE_CURVE('',#2231,#2233,#1382,.T.);
#2698=EDGE_CURVE('',#2233,#2234,#1383,.T.);
#2699=EDGE_CURVE('',#2234,#2232,#1384,.T.);
#2700=EDGE_CURVE('',#2233,#2235,#1385,.T.);
#2701=EDGE_CURVE('',#2235,#2236,#1386,.T.);
#2702=EDGE_CURVE('',#2236,#2234,#1387,.T.);
#2703=EDGE_CURVE('',#2235,#2225,#1388,.T.);
#2704=EDGE_CURVE('',#2228,#2236,#1389,.T.);
#2705=EDGE_CURVE('',#2237,#2237,#1917,.T.);
#2706=EDGE_CURVE('',#2238,#2238,#1918,.T.);
#2707=EDGE_CURVE('',#2239,#2239,#1919,.T.);
#2708=EDGE_CURVE('',#2239,#2238,#1390,.T.);
#2709=EDGE_CURVE('',#2240,#2240,#1920,.T.);
#2710=EDGE_CURVE('',#2240,#2239,#1391,.T.);
#2711=EDGE_CURVE('',#2241,#2241,#1921,.T.);
#2712=EDGE_CURVE('',#2241,#2240,#1392,.T.);
#2713=EDGE_CURVE('',#2242,#2242,#1922,.T.);
#2714=EDGE_CURVE('',#2243,#2243,#1923,.F.);
#2715=EDGE_CURVE('',#2243,#2242,#1393,.T.);
#2716=EDGE_CURVE('',#2237,#2243,#1394,.T.);
#3539=ORIENTED_EDGE('',*,*,#2687,.T.);
#3540=ORIENTED_EDGE('',*,*,#2688,.T.);
#3541=ORIENTED_EDGE('',*,*,#2689,.T.);
#3542=ORIENTED_EDGE('',*,*,#2690,.F.);
#3543=ORIENTED_EDGE('',*,*,#2691,.T.);
#3544=ORIENTED_EDGE('',*,*,#2692,.T.);
#3545=ORIENTED_EDGE('',*,*,#2693,.T.);
#3546=ORIENTED_EDGE('',*,*,#2688,.F.);
#3547=ORIENTED_EDGE('',*,*,#2694,.T.);
#3548=ORIENTED_EDGE('',*,*,#2695,.T.);
#3549=ORIENTED_EDGE('',*,*,#2696,.T.);
#3550=ORIENTED_EDGE('',*,*,#2692,.F.);
#3551=ORIENTED_EDGE('',*,*,#2697,.T.);
#3552=ORIENTED_EDGE('',*,*,#2698,.T.);
#3553=ORIENTED_EDGE('',*,*,#2699,.T.);
#3554=ORIENTED_EDGE('',*,*,#2695,.F.);
#3555=ORIENTED_EDGE('',*,*,#2700,.T.);
#3556=ORIENTED_EDGE('',*,*,#2701,.T.);
#3557=ORIENTED_EDGE('',*,*,#2702,.T.);
#3558=ORIENTED_EDGE('',*,*,#2698,.F.);
#3559=ORIENTED_EDGE('',*,*,#2703,.T.);
#3560=ORIENTED_EDGE('',*,*,#2690,.T.);
#3561=ORIENTED_EDGE('',*,*,#2704,.T.);
#3562=ORIENTED_EDGE('',*,*,#2701,.F.);
#3563=ORIENTED_EDGE('',*,*,#2703,.F.);
#3564=ORIENTED_EDGE('',*,*,#2700,.F.);
#3565=ORIENTED_EDGE('',*,*,#2697,.F.);
#3566=ORIENTED_EDGE('',*,*,#2694,.F.);
#3567=ORIENTED_EDGE('',*,*,#2691,.F.);
#3568=ORIENTED_EDGE('',*,*,#2687,.F.);
#3569=ORIENTED_EDGE('',*,*,#2704,.F.);
#3570=ORIENTED_EDGE('',*,*,#2689,.F.);
#3571=ORIENTED_EDGE('',*,*,#2693,.F.);
#3572=ORIENTED_EDGE('',*,*,#2696,.F.);
#3573=ORIENTED_EDGE('',*,*,#2699,.F.);
#3574=ORIENTED_EDGE('',*,*,#2702,.F.);
#3575=ORIENTED_EDGE('',*,*,#2705,.F.);
#3576=ORIENTED_EDGE('',*,*,#2706,.F.);
#3577=ORIENTED_EDGE('',*,*,#2707,.F.);
#3578=ORIENTED_EDGE('',*,*,#2708,.T.);
#3579=ORIENTED_EDGE('',*,*,#2706,.T.);
#3580=ORIENTED_EDGE('',*,*,#2708,.F.);
#3581=ORIENTED_EDGE('',*,*,#2709,.F.);
#3582=ORIENTED_EDGE('',*,*,#2710,.T.);
#3583=ORIENTED_EDGE('',*,*,#2707,.T.);
#3584=ORIENTED_EDGE('',*,*,#2710,.F.);
#3585=ORIENTED_EDGE('',*,*,#2711,.F.);
#3586=ORIENTED_EDGE('',*,*,#2712,.T.);
#3587=ORIENTED_EDGE('',*,*,#2709,.T.);
#3588=ORIENTED_EDGE('',*,*,#2712,.F.);
#3589=ORIENTED_EDGE('',*,*,#2711,.T.);
#3590=ORIENTED_EDGE('',*,*,#2713,.F.);
#3591=ORIENTED_EDGE('',*,*,#2714,.F.);
#3592=ORIENTED_EDGE('',*,*,#2715,.T.);
#3593=ORIENTED_EDGE('',*,*,#2713,.T.);
#3594=ORIENTED_EDGE('',*,*,#2715,.F.);
#3595=ORIENTED_EDGE('',*,*,#2705,.T.);
#3596=ORIENTED_EDGE('',*,*,#2716,.T.);
#3597=ORIENTED_EDGE('',*,*,#2714,.T.);
#3598=ORIENTED_EDGE('',*,*,#2716,.F.);
#3991=CYLINDRICAL_SURFACE('',#4825,0.425);
#3992=CYLINDRICAL_SURFACE('',#4833,0.24505);
#4167=ADVANCED_FACE('',(#677),#472,.F.);
#4168=ADVANCED_FACE('',(#678),#473,.F.);
#4169=ADVANCED_FACE('',(#679),#474,.F.);
#4170=ADVANCED_FACE('',(#680),#475,.F.);
#4171=ADVANCED_FACE('',(#681),#476,.F.);
#4172=ADVANCED_FACE('',(#682),#477,.F.);
#4173=ADVANCED_FACE('',(#683),#478,.F.);
#4174=ADVANCED_FACE('',(#684),#479,.F.);
#4175=ADVANCED_FACE('',(#685),#480,.F.);
#4176=ADVANCED_FACE('',(#686),#481,.T.);
#4177=ADVANCED_FACE('',(#687),#156,.T.);
#4178=ADVANCED_FACE('',(#688),#3991,.T.);
#4179=ADVANCED_FACE('',(#689),#157,.T.);
#4180=ADVANCED_FACE('',(#690,#329),#482,.T.);
#4181=ADVANCED_FACE('',(#691),#158,.T.);
#4182=ADVANCED_FACE('',(#692),#3992,.T.);
#4297=CLOSED_SHELL('',(#4167,#4168,#4169,#4170,#4171,#4172,#4173,#4174));
#4298=CLOSED_SHELL('',(#4175,#4176,#4177,#4178,#4179,#4180,#4181,#4182));
#4810=AXIS2_PLACEMENT_3D('',#7311,#5748,#5749);
#4811=AXIS2_PLACEMENT_3D('',#7312,#5750,#5751);
#4812=AXIS2_PLACEMENT_3D('',#7321,#5756,#5757);
#4813=AXIS2_PLACEMENT_3D('',#7327,#5761,#5762);
#4814=AXIS2_PLACEMENT_3D('',#7333,#5766,#5767);
#4815=AXIS2_PLACEMENT_3D('',#7339,#5771,#5772);
#4816=AXIS2_PLACEMENT_3D('',#7345,#5776,#5777);
#4817=AXIS2_PLACEMENT_3D('',#7348,#5780,#5781);
#4818=AXIS2_PLACEMENT_3D('',#7349,#5782,#5783);
#4819=AXIS2_PLACEMENT_3D('',#7350,#5784,#5785);
#4820=AXIS2_PLACEMENT_3D('',#7352,#5786,#5787);
#4821=AXIS2_PLACEMENT_3D('',#7353,#5788,#5789);
#4822=AXIS2_PLACEMENT_3D('',#7355,#5790,#5791);
#4823=AXIS2_PLACEMENT_3D('',#7356,#5792,#5793);
#4824=AXIS2_PLACEMENT_3D('',#7358,#5794,#5795);
#4825=AXIS2_PLACEMENT_3D('',#7360,#5797,#5798);
#4826=AXIS2_PLACEMENT_3D('',#7362,#5799,#5800);
#4827=AXIS2_PLACEMENT_3D('',#7364,#5802,#5803);
#4828=AXIS2_PLACEMENT_3D('',#7366,#5804,#5805);
#4829=AXIS2_PLACEMENT_3D('',#7368,#5807,#5808);
#4830=AXIS2_PLACEMENT_3D('',#7370,#5809,#5810);
#4831=AXIS2_PLACEMENT_3D('',#7371,#5811,#5812);
#4832=AXIS2_PLACEMENT_3D('',#7373,#5813,#5814);
#4833=AXIS2_PLACEMENT_3D('',#7375,#5816,#5817);
#5748=DIRECTION('axis',(0.,0.,1.));
#5749=DIRECTION('refdir',(1.,0.,0.));
#5750=DIRECTION('center_axis',(0.866025403784439,0.,-0.5));
#5751=DIRECTION('ref_axis',(0.5,0.,0.866025403784439));
#5752=DIRECTION('',(-0.5,0.,-0.866025403784439));
#5753=DIRECTION('',(0.,-1.,0.));
#5754=DIRECTION('',(0.5,0.,0.866025403784439));
#5755=DIRECTION('',(0.,-1.,0.));
#5756=DIRECTION('center_axis',(1.20185167898973E-16,0.,-1.));
#5757=DIRECTION('ref_axis',(1.,0.,1.20185167898973E-16));
#5758=DIRECTION('',(-1.,0.,-1.20185167898973E-16));
#5759=DIRECTION('',(0.,-1.,0.));
#5760=DIRECTION('',(1.,0.,1.20185167898973E-16));
#5761=DIRECTION('center_axis',(-0.866025403784439,0.,-0.5));
#5762=DIRECTION('ref_axis',(0.5,0.,-0.866025403784439));
#5763=DIRECTION('',(-0.5,0.,0.866025403784439));
#5764=DIRECTION('',(0.,-1.,0.));
#5765=DIRECTION('',(0.5,0.,-0.866025403784439));
#5766=DIRECTION('center_axis',(-0.866025403784439,0.,0.5));
#5767=DIRECTION('ref_axis',(-0.5,0.,-0.866025403784439));
#5768=DIRECTION('',(0.5,0.,0.866025403784439));
#5769=DIRECTION('',(0.,-1.,0.));
#5770=DIRECTION('',(-0.5,0.,-0.866025403784439));
#5771=DIRECTION('center_axis',(-2.40370335797945E-16,0.,1.));
#5772=DIRECTION('ref_axis',(-1.,0.,-2.40370335797945E-16));
#5773=DIRECTION('',(1.,0.,2.40370335797945E-16));
#5774=DIRECTION('',(0.,-1.,0.));
#5775=DIRECTION('',(-1.,0.,-2.40370335797945E-16));
#5776=DIRECTION('center_axis',(0.866025403784439,0.,0.5));
#5777=DIRECTION('ref_axis',(-0.5,0.,0.866025403784439));
#5778=DIRECTION('',(0.5,0.,-0.866025403784439));
#5779=DIRECTION('',(-0.5,0.,0.866025403784439));
#5780=DIRECTION('center_axis',(0.,1.,0.));
#5781=DIRECTION('ref_axis',(1.,0.,0.));
#5782=DIRECTION('center_axis',(0.,-1.,0.));
#5783=DIRECTION('ref_axis',(0.,0.,-1.));
#5784=DIRECTION('center_axis',(0.,1.,0.));
#5785=DIRECTION('ref_axis',(1.,0.,0.));
#5786=DIRECTION('center_axis',(0.,1.,0.));
#5787=DIRECTION('ref_axis',(1.,0.,0.));
#5788=DIRECTION('center_axis',(0.,1.,0.));
#5789=DIRECTION('ref_axis',(0.,0.,1.));
#5790=DIRECTION('center_axis',(0.,-1.,0.));
#5791=DIRECTION('ref_axis',(1.,0.,0.));
#5792=DIRECTION('center_axis',(0.,-1.,0.));
#5793=DIRECTION('ref_axis',(1.,0.,0.));
#5794=DIRECTION('center_axis',(0.,-1.,0.));
#5795=DIRECTION('ref_axis',(1.,0.,0.));
#5796=DIRECTION('',(0.707106781186548,0.707106781186547,8.65956056235493E-17));
#5797=DIRECTION('center_axis',(0.,-1.,0.));
#5798=DIRECTION('ref_axis',(1.,0.,0.));
#5799=DIRECTION('center_axis',(0.,-1.,0.));
#5800=DIRECTION('ref_axis',(1.,0.,0.));
#5801=DIRECTION('',(0.,1.,0.));
#5802=DIRECTION('center_axis',(0.,1.,0.));
#5803=DIRECTION('ref_axis',(1.,0.,0.));
#5804=DIRECTION('center_axis',(0.,-1.,0.));
#5805=DIRECTION('ref_axis',(1.,0.,0.));
#5806=DIRECTION('',(-0.707106781186547,0.707106781186548,-8.65956056235493E-17));
#5807=DIRECTION('center_axis',(0.,-1.,0.));
#5808=DIRECTION('ref_axis',(0.,0.,-1.));
#5809=DIRECTION('center_axis',(0.,-1.,0.));
#5810=DIRECTION('ref_axis',(1.,0.,0.));
#5811=DIRECTION('center_axis',(0.,1.,0.));
#5812=DIRECTION('ref_axis',(1.,0.,0.));
#5813=DIRECTION('center_axis',(0.,1.,0.));
#5814=DIRECTION('ref_axis',(1.,0.,0.));
#5815=DIRECTION('',(-0.447213595499958,0.894427190999916,-5.47678698264203E-17));
#5816=DIRECTION('center_axis',(0.,-1.,0.));
#5817=DIRECTION('ref_axis',(1.,0.,0.));
#5818=DIRECTION('',(0.,1.,0.));
#7311=CARTESIAN_POINT('',(0.,0.,0.));
#7312=CARTESIAN_POINT('Origin',(0.115470053837925,-0.5,-0.2));
#7313=CARTESIAN_POINT('',(0.23094010767585,-0.5,0.));
#7314=CARTESIAN_POINT('',(0.115470053837925,-0.5,-0.2));
#7315=CARTESIAN_POINT('',(0.23094010767585,-0.5,0.));
#7316=CARTESIAN_POINT('',(0.115470053837925,-0.8,-0.2));
#7317=CARTESIAN_POINT('',(0.115470053837925,-0.5,-0.2));
#7318=CARTESIAN_POINT('',(0.23094010767585,-0.8,0.));
#7319=CARTESIAN_POINT('',(0.23094010767585,-0.8,0.));
#7320=CARTESIAN_POINT('',(0.23094010767585,-0.5,0.));
#7321=CARTESIAN_POINT('Origin',(-0.115470053837925,-0.5,-0.2));
#7322=CARTESIAN_POINT('',(-0.115470053837925,-0.5,-0.2));
#7323=CARTESIAN_POINT('',(0.115470053837925,-0.5,-0.2));
#7324=CARTESIAN_POINT('',(-0.115470053837925,-0.8,-0.2));
#7325=CARTESIAN_POINT('',(-0.115470053837925,-0.5,-0.2));
#7326=CARTESIAN_POINT('',(0.115470053837925,-0.8,-0.2));
#7327=CARTESIAN_POINT('Origin',(-0.23094010767585,-0.5,-2.77555756156289E-17));
#7328=CARTESIAN_POINT('',(-0.23094010767585,-0.5,-2.82820063659975E-17));
#7329=CARTESIAN_POINT('',(-0.115470053837925,-0.5,-0.2));
#7330=CARTESIAN_POINT('',(-0.23094010767585,-0.8,-2.77555756156289E-17));
#7331=CARTESIAN_POINT('',(-0.23094010767585,-0.5,-2.82820063659975E-17));
#7332=CARTESIAN_POINT('',(-0.115470053837925,-0.8,-0.2));
#7333=CARTESIAN_POINT('Origin',(-0.115470053837925,-0.5,0.2));
#7334=CARTESIAN_POINT('',(-0.115470053837925,-0.5,0.2));
#7335=CARTESIAN_POINT('',(-0.23094010767585,-0.5,-2.82820063659975E-17));
#7336=CARTESIAN_POINT('',(-0.115470053837925,-0.8,0.2));
#7337=CARTESIAN_POINT('',(-0.115470053837925,-0.5,0.2));
#7338=CARTESIAN_POINT('',(-0.23094010767585,-0.8,-2.82820063659975E-17));
#7339=CARTESIAN_POINT('Origin',(0.115470053837925,-0.5,0.2));
#7340=CARTESIAN_POINT('',(0.115470053837925,-0.5,0.2));
#7341=CARTESIAN_POINT('',(-0.115470053837925,-0.5,0.2));
#7342=CARTESIAN_POINT('',(0.115470053837925,-0.8,0.2));
#7343=CARTESIAN_POINT('',(0.115470053837925,-0.5,0.2));
#7344=CARTESIAN_POINT('',(-0.115470053837925,-0.8,0.2));
#7345=CARTESIAN_POINT('Origin',(0.23094010767585,-0.5,0.));
#7346=CARTESIAN_POINT('',(0.115470053837925,-0.5,0.2));
#7347=CARTESIAN_POINT('',(0.115470053837925,-0.8,0.2));
#7348=CARTESIAN_POINT('Origin',(0.,-0.5,0.));
#7349=CARTESIAN_POINT('Origin',(0.,-0.8,0.));
#7350=CARTESIAN_POINT('Origin',(0.,-1.4,0.));
#7351=CARTESIAN_POINT('',(-0.24505,-1.4,3.00099698131059E-17));
#7352=CARTESIAN_POINT('Origin',(0.,-1.4,0.));
#7353=CARTESIAN_POINT('Origin',(0.375,0.5,0.));
#7354=CARTESIAN_POINT('',(-0.375,0.5,-4.59242549680257E-17));
#7355=CARTESIAN_POINT('Origin',(0.,0.5,0.));
#7356=CARTESIAN_POINT('Origin',(0.,0.475,0.));
#7357=CARTESIAN_POINT('',(-0.425,0.45,-5.20474889637625E-17));
#7358=CARTESIAN_POINT('Origin',(0.,0.45,0.));
#7359=CARTESIAN_POINT('',(-0.4,0.475,-4.89858719658941E-17));
#7360=CARTESIAN_POINT('Origin',(0.,0.24,0.));
#7361=CARTESIAN_POINT('',(-0.425,0.0299999999999998,-5.20474889637625E-17));
#7362=CARTESIAN_POINT('Origin',(0.,0.0299999999999998,0.));
#7363=CARTESIAN_POINT('',(-0.425,0.24,-5.20474889637625E-17));
#7364=CARTESIAN_POINT('Origin',(0.,0.0150000000000001,0.));
#7365=CARTESIAN_POINT('',(-0.395,4.85722573273506E-17,-4.83735485663204E-17));
#7366=CARTESIAN_POINT('Origin',(0.,0.,0.));
#7367=CARTESIAN_POINT('',(-0.41,0.0150000000000001,-5.02105187650415E-17));
#7368=CARTESIAN_POINT('Origin',(0.27,0.,0.));
#7369=CARTESIAN_POINT('',(-0.27,0.,-3.30654635769785E-17));
#7370=CARTESIAN_POINT('Origin',(0.,0.,0.));
#7371=CARTESIAN_POINT('Origin',(0.,-0.02,0.));
#7372=CARTESIAN_POINT('',(-0.24505,-0.0498999999999999,3.00099698131059E-17));
#7373=CARTESIAN_POINT('Origin',(0.,-0.0498999999999999,0.));
#7374=CARTESIAN_POINT('',(-0.26,-0.02,-3.18408167778312E-17));
#7375=CARTESIAN_POINT('Origin',(0.,-0.995,0.));
#7376=CARTESIAN_POINT('',(-0.24505,-0.995,-3.00099698131059E-17));
#7847=UNCERTAINTY_MEASURE_WITH_UNIT(LENGTH_MEASURE(0.001),#7898,
'DISTANCE_ACCURACY_VALUE',
'Maximum model space distance between geometric entities at asserted c
onnectivities');
#7865=UNCERTAINTY_MEASURE_WITH_UNIT(LENGTH_MEASURE(0.001),#7898,
'DISTANCE_ACCURACY_VALUE',
'Maximum model space distance between geometric entities at asserted c
onnectivities');
#7879=(
GEOMETRIC_REPRESENTATION_CONTEXT(3)
GLOBAL_UNCERTAINTY_ASSIGNED_CONTEXT((#7847))
GLOBAL_UNIT_ASSIGNED_CONTEXT((#7898,#7900,#7901))
REPRESENTATION_CONTEXT('','3D')
);
#7897=(
GEOMETRIC_REPRESENTATION_CONTEXT(3)
GLOBAL_UNCERTAINTY_ASSIGNED_CONTEXT((#7865))
GLOBAL_UNIT_ASSIGNED_CONTEXT((#7898,#7900,#7901))
REPRESENTATION_CONTEXT('','3D')
);
#7898=(
LENGTH_UNIT()
NAMED_UNIT(*)
SI_UNIT(.CENTI.,.METRE.)
);
#7900=(
NAMED_UNIT(*)
PLANE_ANGLE_UNIT()
SI_UNIT($,.RADIAN.)
);
#7901=(
NAMED_UNIT(*)
SI_UNIT($,.STERADIAN.)
SOLID_ANGLE_UNIT()
);
#7915=SHAPE_DEFINITION_REPRESENTATION(#7946,#8012);
#7946=PRODUCT_DEFINITION_SHAPE('',$,#8044);
#8012=SHAPE_REPRESENTATION('',(#4810),#7879);
#8030=PRODUCT_DEFINITION_CONTEXT('part definition',#8125,'design');
#8044=PRODUCT_DEFINITION('M5x14 Cap Screw','M5x14 Cap Screw',#8075,#8030);
#8075=PRODUCT_DEFINITION_FORMATION('',$,#8140);
#8125=APPLICATION_CONTEXT(
'Core Data for Automotive Mechanical Design Process');
#8126=PRODUCT_CONTEXT('part definition',#8125,'mechanical');
#8140=PRODUCT('M5x14 Cap Screw','M5x14 Cap Screw','M5x14 Cap Screw',(#8126));
#8221=COLOUR_RGB('Black',0.12,0.14,0.17);
#8222=FILL_AREA_STYLE_COLOUR('',#8221);
#8223=FILL_AREA_STYLE('',(#8222));
#8224=SURFACE_STYLE_FILL_AREA(#8223);
#8225=SURFACE_SIDE_STYLE('',(#8224));
#8226=SURFACE_STYLE_USAGE(.BOTH.,#8225);
#8227=PRESENTATION_STYLE_ASSIGNMENT((#8226));
ENDSEC;
END-ISO-10303-21;
